ISO-10303-21;
HEADER;
FILE_DESCRIPTION (('STEP AP214'),
    '1' );
FILE_NAME ('double end studs bm=1.5d_am_AM A M10X60-N.step',
    '2026-09-30T16:28:02',
    ( '' ),
    ( '' ),
    'SwSTEP 2.0',
    'SolidWorks 2026',
    '' );
FILE_SCHEMA (( 'AUTOMOTIVE_DESIGN' ));
ENDSEC;

DATA;
#21=ADVANCED_BREP_SHAPE_REPRESENTATION ( '', ( #979, #13190 ), #8326 ) ;
#72=( NAMED_UNIT ( * ) PLANE_ANGLE_UNIT ( ) SI_UNIT ( $, .RADIAN. ) );
#88=DIRECTION ( 'NONE',  ( 1.000000000000000000, 0.000000000000000000, 0.000000000000000000 ) ) ;
#151=PRESENTATION_STYLE_ASSIGNMENT (( #9284 ) ) ;
#261=ORIENTED_EDGE ( 'NONE', *, *, #3073, .F. ) ;
#283=CONICAL_SURFACE ( 'NONE', #26615, 4.513000000000000789, 0.2131563744996339549 ) ;
#311=LINE ( 'NONE', #12188, #27806 ) ;
#329=ORIENTED_EDGE ( 'NONE', *, *, #5122, .F. ) ;
#373=DIRECTION ( 'NONE',  ( -1.000000000000000000, -0.000000000000000000, -0.000000000000000000 ) ) ;
#451=FACE_OUTER_BOUND ( 'NONE', #23218, .T. ) ;
#478=VECTOR ( 'NONE', #30246, 1000.000000000000000 ) ;
#586=ORIENTED_EDGE ( 'NONE', *, *, #25073, .T. ) ;
#705=VERTEX_POINT ( 'NONE', #19891 ) ;
#936=SHAPE_DEFINITION_REPRESENTATION ( #13498, #29092 ) ;
#979=MANIFOLD_SOLID_BREP ( 'BaseBody', #6798 ) ;
#982=ORIENTED_EDGE ( 'NONE', *, *, #22137, .F. ) ;
#1024=AXIS2_PLACEMENT_3D ( 'NONE', #17499, #29628, #18407 ) ;
#1251=CIRCLE ( 'NONE', #12936, 5.000000000000000888 ) ;
#1278=EDGE_CURVE ( 'NONE', #14937, #21885, #26548, .T. ) ;
#1325=CIRCLE ( 'NONE', #9068, 4.187999999999997947 ) ;
#1334=LINE ( 'NONE', #4363, #17592 ) ;
#1393=CIRCLE ( 'NONE', #1883, 4.756499999999999062 ) ;
#1501=EDGE_LOOP ( 'NONE', ( #17519, #8441, #11532, #15536 ) ) ;
#1619=DIRECTION ( 'NONE',  ( -1.000000000000000000, 0.000000000000000000, -0.000000000000000000 ) ) ;
#1695=CARTESIAN_POINT ( 'NONE',  ( 74.18800000000001660, -1.387778780781445676E-16, 5.000000000000000888 ) ) ;
#1719=EDGE_CURVE ( 'NONE', #30215, #14810, #16548, .T. ) ;
#1736=CARTESIAN_POINT ( 'NONE',  ( 0.000000000000000000, 0.000000000000000000, 0.000000000000000000 ) ) ;
#1834=ORIENTED_EDGE ( 'NONE', *, *, #1278, .F. ) ;
#1838=AXIS2_PLACEMENT_3D ( 'NONE', #8257, #5982, #8108 ) ;
#1854=DIRECTION ( 'NONE',  ( 0.000000000000000000, -2.775557561562890735E-17, 1.000000000000000000 ) ) ;
#1867=EDGE_LOOP ( 'NONE', ( #10814, #20642 ) ) ;
#1883=AXIS2_PLACEMENT_3D ( 'NONE', #9929, #16804, #25983 ) ;
#1937=CARTESIAN_POINT ( 'NONE',  ( 15.00000000000000000, 0.000000000000000000, 0.000000000000000000 ) ) ;
#2011=DIRECTION ( 'NONE',  ( 0.000000000000000000, -2.775557561562890735E-17, 1.000000000000000000 ) ) ;
#2045=VECTOR ( 'NONE', #18843, 1000.000000000000000 ) ;
#2103=APPLICATION_CONTEXT ( 'automotive_design' ) ;
#2122=ORIENTED_EDGE ( 'NONE', *, *, #3314, .T. ) ;
#2138=CARTESIAN_POINT ( 'NONE',  ( 0.000000000000000000, 0.000000000000000000, 0.000000000000000000 ) ) ;
#2342=CONICAL_SURFACE ( 'NONE', #2821, 4.187999999999997947, 0.7853981633974482790 ) ;
#2380=AXIS2_PLACEMENT_3D ( 'NONE', #13272, #29968, #17691 ) ;
#2411=( GEOMETRIC_REPRESENTATION_CONTEXT ( 3 ) GLOBAL_UNCERTAINTY_ASSIGNED_CONTEXT ( ( #15606 ) ) GLOBAL_UNIT_ASSIGNED_CONTEXT ( ( #25786, #30262, #20888 ) ) REPRESENTATION_CONTEXT ( 'NONE', 'WORKASPACE' ) );
#2454=DIRECTION ( 'NONE',  ( 0.000000000000000000, -2.775557561562890735E-17, 1.000000000000000000 ) ) ;
#2507=CIRCLE ( 'NONE', #25899, 5.000000000000000888 ) ;
#2601=DIRECTION ( 'NONE',  ( 0.000000000000000000, -2.775557561562891351E-17, 1.000000000000000000 ) ) ;
#2615=EDGE_CURVE ( 'NONE', #12978, #22805, #14492, .T. ) ;
#2638=CARTESIAN_POINT ( 'NONE',  ( 0.000000000000000000, 4.350936251500947638E-16, 4.187999999999997058 ) ) ;
#2679=CARTESIAN_POINT ( 'NONE',  ( 49.00000000000000000, 0.000000000000000000, 0.000000000000000000 ) ) ;
#2727=ORIENTED_EDGE ( 'NONE', *, *, #11512, .F. ) ;
#2741=VERTEX_POINT ( 'NONE', #2638 ) ;
#2794=AXIS2_PLACEMENT_3D ( 'NONE', #3031, #11856, #23622 ) ;
#2821=AXIS2_PLACEMENT_3D ( 'NONE', #15628, #6628, #8900 ) ;
#2878=VERTEX_POINT ( 'NONE', #16805 ) ;
#2906=MECHANICAL_DESIGN_GEOMETRIC_PRESENTATION_REPRESENTATION('',(#23841),#2411);
#2946=PRODUCT_DEFINITION_FORMATION_WITH_SPECIFIED_SOURCE ( 'ANY', '', #14920, .NOT_KNOWN. ) ;
#3031=CARTESIAN_POINT ( 'NONE',  ( 0.8120000000000002771, 0.000000000000000000, 0.000000000000000000 ) ) ;
#3073=EDGE_CURVE ( 'NONE', #10747, #2878, #13101, .T. ) ;
#3161=ORIENTED_EDGE ( 'NONE', *, *, #23629, .T. ) ;
#3169=ORIENTED_EDGE ( 'NONE', *, *, #24776, .T. ) ;
#3175=CIRCLE ( 'NONE', #8990, 4.756499999999999950 ) ;
#3314=EDGE_CURVE ( 'NONE', #4331, #14937, #11614, .T. ) ;
#3348=EDGE_CURVE ( 'NONE', #16128, #5097, #12599, .T. ) ;
#3362=AXIS2_PLACEMENT_3D ( 'NONE', #27447, #17924, #15493 ) ;
#3397=AXIS2_PLACEMENT_3D ( 'NONE', #26209, #10457, #24515 ) ;
#3438=DIRECTION ( 'NONE',  ( 1.000000000000000000, 0.000000000000000000, 0.000000000000000000 ) ) ;
#3571=EDGE_CURVE ( 'NONE', #30215, #16128, #28205, .T. ) ;
#3592=DIRECTION ( 'NONE',  ( 0.000000000000000000, -2.775557561562890735E-17, 1.000000000000000000 ) ) ;
#3636=ORIENTED_EDGE ( 'NONE', *, *, #29447, .F. ) ;
#3673=CYLINDRICAL_SURFACE ( 'NONE', #26664, 5.000000000000000000 ) ;
#3693=FACE_OUTER_BOUND ( 'NONE', #28279, .T. ) ;
#3722=DIRECTION ( 'NONE',  ( 1.000000000000000000, 0.000000000000000000, 0.000000000000000000 ) ) ;
#3822=CARTESIAN_POINT ( 'NONE',  ( 49.00000000000000000, 7.511012776518210972E-16, -5.000000000000000000 ) ) ;
#3829=DIRECTION ( 'NONE',  ( -1.000000000000000000, 0.000000000000000000, -0.000000000000000000 ) ) ;
#4061=ADVANCED_FACE ( 'NONE', ( #8526 ), #27197, .T. ) ;
#4073=EDGE_LOOP ( 'NONE', ( #23882, #2122, #15313, #3161 ) ) ;
#4096=CARTESIAN_POINT ( 'NONE',  ( 13.87499999999999822, -1.353986367469417343E-16, 4.756499999999999062 ) ) ;
#4111=EDGE_LOOP ( 'NONE', ( #28436, #8671, #25897, #23439 ) ) ;
#4158=CONICAL_SURFACE ( 'NONE', #26103, 4.513000000000000789, 0.2131563744996338439 ) ;
#4300=ORIENTED_EDGE ( 'NONE', *, *, #24180, .F. ) ;
#4331=VERTEX_POINT ( 'NONE', #17055 ) ;
#4353=DIRECTION ( 'NONE',  ( 0.000000000000000000, -2.775557561562890735E-17, 1.000000000000000000 ) ) ;
#4363=CARTESIAN_POINT ( 'NONE',  ( 15.00000000000000000, 1.387778780781445429E-16, -5.000000000000000000 ) ) ;
#4436=FACE_OUTER_BOUND ( 'NONE', #1501, .T. ) ;
#4438=ADVANCED_FACE ( 'NONE', ( #19783 ), #18047, .T. ) ;
#4446=DIRECTION ( 'NONE',  ( -1.000000000000000000, 0.000000000000000000, -0.000000000000000000 ) ) ;
#4580=DIRECTION ( 'NONE',  ( -1.000000000000000000, 0.000000000000000000, -0.000000000000000000 ) ) ;
#4621=ORIENTED_EDGE ( 'NONE', *, *, #24776, .F. ) ;
#4760=DIRECTION ( 'NONE',  ( 1.000000000000000000, -0.000000000000000000, 0.000000000000000000 ) ) ;
#4809=DIRECTION ( 'NONE',  ( -1.000000000000000000, 0.000000000000000000, -0.000000000000000000 ) ) ;
#4869=CARTESIAN_POINT ( 'NONE',  ( 75.00000000000000000, 0.000000000000000000, 0.000000000000000000 ) ) ;
#4961=FACE_OUTER_BOUND ( 'NONE', #17966, .T. ) ;
#5097=VERTEX_POINT ( 'NONE', #27596 ) ;
#5103=CARTESIAN_POINT ( 'NONE',  ( 13.87499999999999822, 0.000000000000000000, 0.000000000000000000 ) ) ;
#5121=EDGE_CURVE ( 'NONE', #14937, #4331, #2507, .T. ) ;
#5122=EDGE_CURVE ( 'NONE', #14810, #5097, #1334, .T. ) ;
#5248=EDGE_LOOP ( 'NONE', ( #12189, #9231, #17662, #329 ) ) ;
#5358=VECTOR ( 'NONE', #6315, 1000.000000000000114 ) ;
#5393=ORIENTED_EDGE ( 'NONE', *, *, #19857, .F. ) ;
#5418=DIRECTION ( 'NONE',  ( 0.000000000000000000, -2.775557561562890735E-17, 1.000000000000000000 ) ) ;
#5435=CARTESIAN_POINT ( 'NONE',  ( 0.000000000000000000, 0.000000000000000000, 0.000000000000000000 ) ) ;
#5653=ORIENTED_EDGE ( 'NONE', *, *, #13100, .F. ) ;
#5656=ORIENTED_EDGE ( 'NONE', *, *, #21765, .F. ) ;
#5800=LINE ( 'NONE', #24270, #6205 ) ;
#5965=CARTESIAN_POINT ( 'NONE',  ( 0.000000000000000000, 3.966417288046574668E-16, 4.187999999999997947 ) ) ;
#5982=DIRECTION ( 'NONE',  ( -1.000000000000000000, 0.000000000000000000, -0.000000000000000000 ) ) ;
#5983=DIRECTION ( 'NONE',  ( -1.000000000000000000, 0.000000000000000000, -0.000000000000000000 ) ) ;
#6154=FILL_AREA_STYLE ('',( #20035 ) ) ;
#6186=CONICAL_SURFACE ( 'NONE', #10541, 5.000000000000000000, 0.2131563744996336218 ) ;
#6205=VECTOR ( 'NONE', #17238, 1000.000000000000000 ) ;
#6232=EDGE_CURVE ( 'NONE', #10747, #16128, #17859, .T. ) ;
#6250=CARTESIAN_POINT ( 'NONE',  ( -1.310841663519413114, 0.000000000000000000, 0.000000000000000000 ) ) ;
#6267=DIRECTION ( 'NONE',  ( 0.000000000000000000, -2.775557561562890735E-17, 1.000000000000000000 ) ) ;
#6311=DIRECTION ( 'NONE',  ( 0.000000000000000000, -2.775557561562890735E-17, 1.000000000000000000 ) ) ;
#6315=DIRECTION ( 'NONE',  ( -0.9773680663943724589, 3.177847737406116550E-17, -0.2115458881484710285 ) ) ;
#6348=ORIENTED_EDGE ( 'NONE', *, *, #11037, .T. ) ;
#6404=MECHANICAL_DESIGN_GEOMETRIC_PRESENTATION_REPRESENTATION('',(#24857),#24927);
#6439=ADVANCED_FACE ( 'NONE', ( #14183 ), #20753, .T. ) ;
#6444=ORIENTED_EDGE ( 'NONE', *, *, #14851, .F. ) ;
#6610=LINE ( 'NONE', #18198, #8612 ) ;
#6614=CONICAL_SURFACE ( 'NONE', #25628, 5.000000000000000888, 0.2131563744996338439 ) ;
#6628=DIRECTION ( 'NONE',  ( 1.000000000000000000, 0.000000000000000000, 0.000000000000000000 ) ) ;
#6772=ORIENTED_EDGE ( 'NONE', *, *, #3348, .F. ) ;
#6798=CLOSED_SHELL ( 'NONE', ( #21266, #4061, #12742, #6439, #21342, #24110, #25546, #11795, #26786, #21093, #25212, #17075, #18523, #19902, #20814, #21936, #25449, #4438, #8867, #21278 ) ) ;
#6886=CARTESIAN_POINT ( 'NONE',  ( 49.00000000000000000, 0.000000000000000000, 0.000000000000000000 ) ) ;
#6968=EDGE_LOOP ( 'NONE', ( #4621, #6348, #23415, #5393 ) ) ;
#6988=CARTESIAN_POINT ( 'NONE',  ( 47.87499999999999289, -1.320193954157388764E-16, 4.756499999999999062 ) ) ;
#6994=CARTESIAN_POINT ( 'NONE',  ( 49.00000000000000000, 1.387778780781445676E-16, -5.000000000000000888 ) ) ;
#7003=DIRECTION ( 'NONE',  ( 1.000000000000000000, 0.000000000000000000, 0.000000000000000000 ) ) ;
#7004=ORIENTED_EDGE ( 'NONE', *, *, #1719, .T. ) ;
#7057=AXIS2_PLACEMENT_3D ( 'NONE', #8583, #3722, #22494 ) ;
#7149=PLANE ( 'NONE',  #19827 ) ;
#7164=VECTOR ( 'NONE', #10819, 1000.000000000000000 ) ;
#7223=AXIS2_PLACEMENT_3D ( 'NONE', #29606, #8767, #4353 ) ;
#7232=AXIS2_PLACEMENT_3D ( 'NONE', #17835, #22741, #1854 ) ;
#7396=ORIENTED_EDGE ( 'NONE', *, *, #29401, .F. ) ;
#7530=SURFACE_STYLE_FILL_AREA ( #9661 ) ;
#7546=LINE ( 'NONE', #28195, #12614 ) ;
#7650=ORIENTED_EDGE ( 'NONE', *, *, #19817, .F. ) ;
#7792=ORIENTED_EDGE ( 'NONE', *, *, #5121, .F. ) ;
#8009=CARTESIAN_POINT ( 'NONE',  ( 75.00000000000000000, 5.000000000000000000, -1.084202172485504434E-15 ) ) ;
#8108=DIRECTION ( 'NONE',  ( 0.000000000000000000, -2.775557561562890735E-17, 1.000000000000000000 ) ) ;
#8178=CARTESIAN_POINT ( 'NONE',  ( 46.75000000000000000, -1.387778780781445676E-16, 5.000000000000000888 ) ) ;
#8223=ORIENTED_EDGE ( 'NONE', *, *, #12974, .F. ) ;
#8257=CARTESIAN_POINT ( 'NONE',  ( -1.310841663519413114, 0.000000000000000000, 0.000000000000000000 ) ) ;
#8326=( GEOMETRIC_REPRESENTATION_CONTEXT ( 3 ) GLOBAL_UNCERTAINTY_ASSIGNED_CONTEXT ( ( #18658 ) ) GLOBAL_UNIT_ASSIGNED_CONTEXT ( ( #15634, #16691, #18824 ) ) REPRESENTATION_CONTEXT ( 'NONE', 'WORKASPACE' ) );
#8441=ORIENTED_EDGE ( 'NONE', *, *, #12974, .T. ) ;
#8478=CARTESIAN_POINT ( 'NONE',  ( 49.00000000000000000, 6.779440132085338567E-16, -4.513000000000000789 ) ) ;
#8526=FACE_OUTER_BOUND ( 'NONE', #9267, .T. ) ;
#8576=AXIS2_PLACEMENT_3D ( 'NONE', #27121, #1619, #17617 ) ;
#8583=CARTESIAN_POINT ( 'NONE',  ( 15.00000000000000000, 0.000000000000000000, 0.000000000000000000 ) ) ;
#8612=VECTOR ( 'NONE', #23095, 1000.000000000000114 ) ;
#8631=DIRECTION ( 'NONE',  ( -1.000000000000000000, 0.000000000000000000, -0.000000000000000000 ) ) ;
#8671=ORIENTED_EDGE ( 'NONE', *, *, #1719, .F. ) ;
#8686=LINE ( 'NONE', #5965, #14914 ) ;
#8707=ORIENTED_EDGE ( 'NONE', *, *, #24180, .T. ) ;
#8751=ORIENTED_EDGE ( 'NONE', *, *, #10348, .T. ) ;
#8753=LINE ( 'NONE', #20510, #13949 ) ;
#8767=DIRECTION ( 'NONE',  ( -1.000000000000000000, 0.000000000000000000, -0.000000000000000000 ) ) ;
#8867=ADVANCED_FACE ( 'NONE', ( #451 ), #23800, .T. ) ;
#8883=CARTESIAN_POINT ( 'NONE',  ( 15.00000000000000000, 6.779440132085338567E-16, -4.513000000000000789 ) ) ;
#8900=DIRECTION ( 'NONE',  ( 0.000000000000000000, 2.775557561562890735E-17, -1.000000000000000000 ) ) ;
#8920=VECTOR ( 'NONE', #27491, 1000.000000000000114 ) ;
#8990=AXIS2_PLACEMENT_3D ( 'NONE', #5103, #14697, #24038 ) ;
#9068=AXIS2_PLACEMENT_3D ( 'NONE', #11942, #373, #26012 ) ;
#9117=AXIS2_PLACEMENT_3D ( 'NONE', #8009, #20207, #3592 ) ;
#9134=CARTESIAN_POINT ( 'NONE',  ( 46.75000000000000000, 0.000000000000000000, 0.000000000000000000 ) ) ;
#9231=ORIENTED_EDGE ( 'NONE', *, *, #3571, .T. ) ;
#9267=EDGE_LOOP ( 'NONE', ( #8707, #11261, #7396, #21217 ) ) ;
#9284=SURFACE_STYLE_USAGE ( .BOTH. , #9431 ) ;
#9305=PRODUCT_DEFINITION ( 'UNKNOWN', '', #2946, #17406 ) ;
#9311=VERTEX_POINT ( 'NONE', #6988 ) ;
#9431=SURFACE_SIDE_STYLE ('',( #15451 ) ) ;
#9439=ORIENTED_EDGE ( 'NONE', *, *, #13100, .T. ) ;
#9661=FILL_AREA_STYLE ('',( #25705 ) ) ;
#9721=EDGE_CURVE ( 'NONE', #9725, #2878, #15188, .T. ) ;
#9725=VERTEX_POINT ( 'NONE', #29460 ) ;
#9795=EDGE_CURVE ( 'NONE', #14810, #4331, #25080, .T. ) ;
#9929=CARTESIAN_POINT ( 'NONE',  ( 47.87499999999999289, 0.000000000000000000, 0.000000000000000000 ) ) ;
#9982=CARTESIAN_POINT ( 'NONE',  ( 46.75000000000000000, 0.000000000000000000, 0.000000000000000000 ) ) ;
#10014=DIRECTION ( 'NONE',  ( -1.000000000000000000, 0.000000000000000000, -0.000000000000000000 ) ) ;
#10037=AXIS2_PLACEMENT_3D ( 'NONE', #21701, #5983, #14673 ) ;
#10179=EDGE_LOOP ( 'NONE', ( #18600, #7004, #12684, #20865 ) ) ;
#10233=CIRCLE ( 'NONE', #29297, 5.000000000000000888 ) ;
#10348=EDGE_CURVE ( 'NONE', #9725, #26738, #18125, .T. ) ;
#10446=DIRECTION ( 'NONE',  ( 1.000000000000000000, 0.000000000000000000, 0.000000000000000000 ) ) ;
#10457=DIRECTION ( 'NONE',  ( 1.000000000000000000, 0.000000000000000000, 0.000000000000000000 ) ) ;
#10496=ORIENTED_EDGE ( 'NONE', *, *, #23011, .T. ) ;
#10541=AXIS2_PLACEMENT_3D ( 'NONE', #21409, #19116, #25691 ) ;
#10747=VERTEX_POINT ( 'NONE', #8178 ) ;
#10814=ORIENTED_EDGE ( 'NONE', *, *, #26789, .T. ) ;
#10819=DIRECTION ( 'NONE',  ( -1.000000000000000000, 0.000000000000000000, -0.000000000000000000 ) ) ;
#11037=EDGE_CURVE ( 'NONE', #2878, #10747, #1251, .T. ) ;
#11072=DIRECTION ( 'NONE',  ( 0.000000000000000000, -2.775557561562890735E-17, 1.000000000000000000 ) ) ;
#11142=AXIS2_PLACEMENT_3D ( 'NONE', #9134, #4580, #2011 ) ;
#11214=AXIS2_PLACEMENT_3D ( 'NONE', #6250, #15546, #22581 ) ;
#11237=ORIENTED_EDGE ( 'NONE', *, *, #15060, .T. ) ;
#11261=ORIENTED_EDGE ( 'NONE', *, *, #29173, .T. ) ;
#11287=CARTESIAN_POINT ( 'NONE',  ( -1.310841663519413114, 0.000000000000000000, 0.000000000000000000 ) ) ;
#11323=AXIS2_PLACEMENT_3D ( 'NONE', #12027, #23335, #2454 ) ;
#11372=DIRECTION ( 'NONE',  ( -0.9773680663943724589, -5.871577894680262505E-18, 0.2115458881484710285 ) ) ;
#11442=DIRECTION ( 'NONE',  ( 0.000000000000000000, -2.775557561562890735E-17, 1.000000000000000000 ) ) ;
#11445=EDGE_CURVE ( 'NONE', #26738, #25636, #22561, .T. ) ;
#11491=( NAMED_UNIT ( * ) SI_UNIT ( $, .STERADIAN. ) SOLID_ANGLE_UNIT ( ) );
#11501=CARTESIAN_POINT ( 'NONE',  ( 74.18800000000001660, 7.511012776518211958E-16, -5.000000000000000888 ) ) ;
#11512=EDGE_CURVE ( 'NONE', #20403, #25256, #27196, .T. ) ;
#11532=ORIENTED_EDGE ( 'NONE', *, *, #28701, .T. ) ;
#11614=CIRCLE ( 'NONE', #3362, 5.000000000000000888 ) ;
#11666=CARTESIAN_POINT ( 'NONE',  ( 15.00000000000000000, 4.735455214955320607E-16, 5.000000000000000000 ) ) ;
#11795=ADVANCED_FACE ( 'NONE', ( #3693 ), #26920, .T. ) ;
#11856=DIRECTION ( 'NONE',  ( 1.000000000000000000, 0.000000000000000000, 0.000000000000000000 ) ) ;
#11942=CARTESIAN_POINT ( 'NONE',  ( 0.000000000000000000, 0.000000000000000000, 0.000000000000000000 ) ) ;
#11952=DIRECTION ( 'NONE',  ( 0.7071067811865474617, 1.962615573354718650E-17, -0.7071067811865475727 ) ) ;
#11994=CIRCLE ( 'NONE', #8576, 4.756499999999999062 ) ;
#12027=CARTESIAN_POINT ( 'NONE',  ( -1.310841663519413114, 0.000000000000000000, 0.000000000000000000 ) ) ;
#12088=DIRECTION ( 'NONE',  ( 0.000000000000000000, -2.775557561562890735E-17, 1.000000000000000000 ) ) ;
#12105=SURFACE_SIDE_STYLE ('',( #7530 ) ) ;
#12188=CARTESIAN_POINT ( 'NONE',  ( 49.00000000000000000, -1.252609127533332839E-16, 4.513000000000000789 ) ) ;
#12189=ORIENTED_EDGE ( 'NONE', *, *, #19817, .T. ) ;
#12229=CARTESIAN_POINT ( 'NONE',  ( 74.18800000000001660, 7.511012776518211958E-16, -5.000000000000000888 ) ) ;
#12507=ORIENTED_EDGE ( 'NONE', *, *, #21765, .T. ) ;
#12599=CIRCLE ( 'NONE', #22861, 5.000000000000000000 ) ;
#12614=VECTOR ( 'NONE', #11952, 1000.000000000000000 ) ;
#12667=PRODUCT_CONTEXT ( 'NONE', #13575, 'mechanical' ) ;
#12684=ORIENTED_EDGE ( 'NONE', *, *, #5122, .T. ) ;
#12731=DIRECTION ( 'NONE',  ( 0.000000000000000000, 2.775557561562890735E-17, -1.000000000000000000 ) ) ;
#12737=FACE_OUTER_BOUND ( 'NONE', #21414, .T. ) ;
#12742=ADVANCED_FACE ( 'NONE', ( #13354 ), #18910, .T. ) ;
#12762=DIRECTION ( 'NONE',  ( 0.000000000000000000, -2.775557561562890735E-17, 1.000000000000000000 ) ) ;
#12784=DIRECTION ( 'NONE',  ( -1.000000000000000000, 0.000000000000000000, -0.000000000000000000 ) ) ;
#12936=AXIS2_PLACEMENT_3D ( 'NONE', #9982, #4809, #26340 ) ;
#12974=EDGE_CURVE ( 'NONE', #9725, #9311, #1393, .T. ) ;
#12978=VERTEX_POINT ( 'NONE', #28914 ) ;
#13020=CARTESIAN_POINT ( 'NONE',  ( 15.00000000000000000, 0.000000000000000000, 0.000000000000000000 ) ) ;
#13086=CARTESIAN_POINT ( 'NONE',  ( -1.310841663519413114, 0.000000000000000000, 0.000000000000000000 ) ) ;
#13100=EDGE_CURVE ( 'NONE', #22805, #20403, #26586, .T. ) ;
#13101=CIRCLE ( 'NONE', #11142, 5.000000000000000888 ) ;
#13190=AXIS2_PLACEMENT_3D ( 'NONE', #5435, #19606, #10446 ) ;
#13272=CARTESIAN_POINT ( 'NONE',  ( 0.000000000000000000, 0.000000000000000000, 0.000000000000000000 ) ) ;
#13354=FACE_OUTER_BOUND ( 'NONE', #22549, .T. ) ;
#13419=DIRECTION ( 'NONE',  ( 0.7071067811865474617, 6.696944989000215441E-17, 0.7071067811865475727 ) ) ;
#13498=PRODUCT_DEFINITION_SHAPE ( 'NONE', 'NONE',  #9305 ) ;
#13575=APPLICATION_CONTEXT ( 'automotive_design' ) ;
#13579=VECTOR ( 'NONE', #22219, 1000.000000000000114 ) ;
#13587=ORIENTED_EDGE ( 'NONE', *, *, #3073, .T. ) ;
#13665=CARTESIAN_POINT ( 'NONE',  ( 12.74999999999999822, 0.000000000000000000, 0.000000000000000000 ) ) ;
#13732=DIRECTION ( 'NONE',  ( -1.000000000000000000, 0.000000000000000000, -0.000000000000000000 ) ) ;
#13758=DIRECTION ( 'NONE',  ( 0.000000000000000000, -2.775557561562891351E-17, 1.000000000000000000 ) ) ;
#13949=VECTOR ( 'NONE', #30189, 1000.000000000000000 ) ;
#14068=CARTESIAN_POINT ( 'NONE',  ( 74.18800000000001660, 0.000000000000000000, 0.000000000000000000 ) ) ;
#14166=DIRECTION ( 'NONE',  ( 1.000000000000000000, -0.000000000000000000, 0.000000000000000000 ) ) ;
#14171=DIRECTION ( 'NONE',  ( -0.9773680663943724589, -5.871577894680259423E-18, 0.2115458881484709175 ) ) ;
#14183=FACE_OUTER_BOUND ( 'NONE', #28031, .T. ) ;
#14251=CARTESIAN_POINT ( 'NONE',  ( 49.00000000000000000, 0.000000000000000000, 0.000000000000000000 ) ) ;
#14492=CIRCLE ( 'NONE', #28192, 4.188000000000025480 ) ;
#14673=DIRECTION ( 'NONE',  ( 0.000000000000000000, -2.775557561562890735E-17, 1.000000000000000000 ) ) ;
#14697=DIRECTION ( 'NONE',  ( 1.000000000000000000, 0.000000000000000000, 0.000000000000000000 ) ) ;
#14810=VERTEX_POINT ( 'NONE', #15021 ) ;
#14834=CIRCLE ( 'NONE', #21682, 5.000000000000000000 ) ;
#14851=EDGE_CURVE ( 'NONE', #9311, #9725, #11994, .T. ) ;
#14872=AXIS2_PLACEMENT_3D ( 'NONE', #2679, #88, #27898 ) ;
#14893=VECTOR ( 'NONE', #18152, 1000.000000000000114 ) ;
#14914=VECTOR ( 'NONE', #13419, 1000.000000000000000 ) ;
#14920=PRODUCT ( 'double end studs bm=1.5d_am_AM A M10X60-N', 'double end studs bm=1.5d_am_AM A M10X60-N', '', ( #12667 ) ) ;
#14937=VERTEX_POINT ( 'NONE', #17468 ) ;
#15012=CARTESIAN_POINT ( 'NONE',  ( 0.8120000000000002771, 0.000000000000000000, 0.000000000000000000 ) ) ;
#15021=CARTESIAN_POINT ( 'NONE',  ( 13.87499999999999822, 7.328119615409992624E-16, -4.756499999999999062 ) ) ;
#15060=EDGE_CURVE ( 'NONE', #4331, #705, #8753, .T. ) ;
#15062=DIRECTION ( 'NONE',  ( -1.000000000000000000, 0.000000000000000000, -0.000000000000000000 ) ) ;
#15188=LINE ( 'NONE', #8478, #13579 ) ;
#15294=EDGE_CURVE ( 'NONE', #2741, #23064, #1325, .T. ) ;
#15307=ORIENTED_EDGE ( 'NONE', *, *, #22137, .T. ) ;
#15313=ORIENTED_EDGE ( 'NONE', *, *, #1278, .T. ) ;
#15428=CARTESIAN_POINT ( 'NONE',  ( -1.310841663519413114, -1.387778780781445429E-16, 5.000000000000000000 ) ) ;
#15451=SURFACE_STYLE_FILL_AREA ( #6154 ) ;
#15493=DIRECTION ( 'NONE',  ( 0.000000000000000000, -2.775557561562890735E-17, 1.000000000000000000 ) ) ;
#15516=CIRCLE ( 'NONE', #2380, 4.187999999999997947 ) ;
#15528=DIRECTION ( 'NONE',  ( 0.000000000000000000, -2.775557561562890735E-17, 1.000000000000000000 ) ) ;
#15536=ORIENTED_EDGE ( 'NONE', *, *, #11037, .F. ) ;
#15546=DIRECTION ( 'NONE',  ( -1.000000000000000000, 0.000000000000000000, -0.000000000000000000 ) ) ;
#15605=DIRECTION ( 'NONE',  ( -1.000000000000000000, 0.000000000000000000, -0.000000000000000000 ) ) ;
#15606=UNCERTAINTY_MEASURE_WITH_UNIT (LENGTH_MEASURE( 1.000000000000000082E-05 ), #25786, 'distance_accuracy_value', 'NONE');
#15628=CARTESIAN_POINT ( 'NONE',  ( 0.000000000000000000, 0.000000000000000000, 0.000000000000000000 ) ) ;
#15634=( LENGTH_UNIT ( ) NAMED_UNIT ( * ) SI_UNIT ( .MILLI., .METRE. ) );
#15700=LINE ( 'NONE', #29962, #7164 ) ;
#15790=DIRECTION ( 'NONE',  ( -1.000000000000000000, 0.000000000000000000, -0.000000000000000000 ) ) ;
#15795=DIRECTION ( 'NONE',  ( -1.000000000000000000, 0.000000000000000000, -0.000000000000000000 ) ) ;
#15929=CIRCLE ( 'NONE', #2794, 5.000000000000000888 ) ;
#16128=VERTEX_POINT ( 'NONE', #26239 ) ;
#16149=DIRECTION ( 'NONE',  ( 0.000000000000000000, 2.775557561562890735E-17, -1.000000000000000000 ) ) ;
#16538=( LENGTH_UNIT ( ) NAMED_UNIT ( * ) SI_UNIT ( .MILLI., .METRE. ) );
#16548=CIRCLE ( 'NONE', #3397, 4.756499999999999950 ) ;
#16604=CARTESIAN_POINT ( 'NONE',  ( 74.18800000000001660, -1.387778780781445676E-16, 5.000000000000000888 ) ) ;
#16642=ORIENTED_EDGE ( 'NONE', *, *, #15294, .F. ) ;
#16691=( NAMED_UNIT ( * ) PLANE_ANGLE_UNIT ( ) SI_UNIT ( $, .RADIAN. ) );
#16714=CARTESIAN_POINT ( 'NONE',  ( 49.00000000000000000, 0.000000000000000000, 0.000000000000000000 ) ) ;
#16804=DIRECTION ( 'NONE',  ( -1.000000000000000000, 0.000000000000000000, -0.000000000000000000 ) ) ;
#16805=CARTESIAN_POINT ( 'NONE',  ( 46.75000000000000000, 7.511012776518212944E-16, -5.000000000000000888 ) ) ;
#16892=LINE ( 'NONE', #18882, #478 ) ;
#16906=AXIS2_PLACEMENT_3D ( 'NONE', #14068, #21250, #12088 ) ;
#17055=CARTESIAN_POINT ( 'NONE',  ( 12.74999999999999822, 7.511012776518213930E-16, -5.000000000000000888 ) ) ;
#17069=CARTESIAN_POINT ( 'NONE',  ( -1.310841663519413114, -1.387778780781445676E-16, 5.000000000000000888 ) ) ;
#17075=ADVANCED_FACE ( 'NONE', ( #22100 ), #17663, .T. ) ;
#17132=EDGE_LOOP ( 'NONE', ( #30072, #25304, #261, #23833 ) ) ;
#17184=AXIS2_PLACEMENT_3D ( 'NONE', #20640, #30023, #27713 ) ;
#17198=LINE ( 'NONE', #27599, #17537 ) ;
#17238=DIRECTION ( 'NONE',  ( -1.000000000000000000, 0.000000000000000000, -0.000000000000000000 ) ) ;
#17345=CONICAL_SURFACE ( 'NONE', #22234, 4.513000000000000789, 0.2131563744996338439 ) ;
#17406=PRODUCT_DEFINITION_CONTEXT ( 'detailed design', #2103, 'design' ) ;
#17417=ORIENTED_EDGE ( 'NONE', *, *, #27590, .F. ) ;
#17421=ORIENTED_EDGE ( 'NONE', *, *, #27590, .T. ) ;
#17468=CARTESIAN_POINT ( 'NONE',  ( 12.74999999999999822, -1.387778780781445676E-16, 5.000000000000000888 ) ) ;
#17499=CARTESIAN_POINT ( 'NONE',  ( 74.18800000000001660, 0.000000000000000000, 0.000000000000000000 ) ) ;
#17519=ORIENTED_EDGE ( 'NONE', *, *, #9721, .F. ) ;
#17537=VECTOR ( 'NONE', #11372, 1000.000000000000114 ) ;
#17592=VECTOR ( 'NONE', #20088, 1000.000000000000000 ) ;
#17617=DIRECTION ( 'NONE',  ( 0.000000000000000000, -2.775557561562890735E-17, 1.000000000000000000 ) ) ;
#17662=ORIENTED_EDGE ( 'NONE', *, *, #3348, .T. ) ;
#17663=CYLINDRICAL_SURFACE ( 'NONE', #26482, 5.000000000000000888 ) ;
#17691=DIRECTION ( 'NONE',  ( 0.000000000000000000, 2.775557561562890735E-17, -1.000000000000000000 ) ) ;
#17718=ORIENTED_EDGE ( 'NONE', *, *, #29961, .F. ) ;
#17835=CARTESIAN_POINT ( 'NONE',  ( 15.00000000000000000, 0.000000000000000000, 0.000000000000000000 ) ) ;
#17859=LINE ( 'NONE', #15428, #25386 ) ;
#17924=DIRECTION ( 'NONE',  ( -1.000000000000000000, 0.000000000000000000, -0.000000000000000000 ) ) ;
#17966=EDGE_LOOP ( 'NONE', ( #6444, #15307, #19730, #22351 ) ) ;
#18019=DIRECTION ( 'NONE',  ( -1.000000000000000000, 0.000000000000000000, -0.000000000000000000 ) ) ;
#18047=CONICAL_SURFACE ( 'NONE', #1024, 5.000000000000000888, 0.7853981633974456145 ) ;
#18125=LINE ( 'NONE', #6994, #8920 ) ;
#18152=DIRECTION ( 'NONE',  ( -0.7071067811865492381, -1.962615573354713720E-17, 0.7071067811865457964 ) ) ;
#18198=CARTESIAN_POINT ( 'NONE',  ( 49.00000000000000000, 4.735455214955321593E-16, 5.000000000000000888 ) ) ;
#18387=DIRECTION ( 'NONE',  ( 0.000000000000000000, -2.775557561562890735E-17, 1.000000000000000000 ) ) ;
#18399=ORIENTED_EDGE ( 'NONE', *, *, #26789, .F. ) ;
#18407=DIRECTION ( 'NONE',  ( 0.000000000000000000, -2.775557561562890735E-17, 1.000000000000000000 ) ) ;
#18467=DIRECTION ( 'NONE',  ( 0.000000000000000000, -2.775557561562890735E-17, 1.000000000000000000 ) ) ;
#18488=VECTOR ( 'NONE', #15062, 1000.000000000000000 ) ;
#18523=ADVANCED_FACE ( 'NONE', ( #25487 ), #26521, .T. ) ;
#18571=ORIENTED_EDGE ( 'NONE', *, *, #5121, .T. ) ;
#18600=ORIENTED_EDGE ( 'NONE', *, *, #3571, .F. ) ;
#18658=UNCERTAINTY_MEASURE_WITH_UNIT (LENGTH_MEASURE( 1.000000000000000082E-05 ), #15634, 'distance_accuracy_value', 'NONE');
#18699=ORIENTED_EDGE ( 'NONE', *, *, #2615, .F. ) ;
#18824=( NAMED_UNIT ( * ) SI_UNIT ( $, .STERADIAN. ) SOLID_ANGLE_UNIT ( ) );
#18843=DIRECTION ( 'NONE',  ( 0.9773680663943725699, 2.003532158470061275E-17, 0.2115458881484706954 ) ) ;
#18882=CARTESIAN_POINT ( 'NONE',  ( -1.310841663519413114, 7.511012776518212944E-16, -5.000000000000000888 ) ) ;
#18910=CONICAL_SURFACE ( 'NONE', #7223, 5.000000000000000888, 0.7853981633974456145 ) ;
#19116=DIRECTION ( 'NONE',  ( 1.000000000000000000, 0.000000000000000000, 0.000000000000000000 ) ) ;
#19130=ORIENTED_EDGE ( 'NONE', *, *, #29961, .T. ) ;
#19391=DIRECTION ( 'NONE',  ( -0.7071067811865492381, 1.062217613570962316E-16, -0.7071067811865457964 ) ) ;
#19606=DIRECTION ( 'NONE',  ( 0.000000000000000000, 0.000000000000000000, 1.000000000000000000 ) ) ;
#19730=ORIENTED_EDGE ( 'NONE', *, *, #29401, .T. ) ;
#19783=FACE_OUTER_BOUND ( 'NONE', #26756, .T. ) ;
#19817=EDGE_CURVE ( 'NONE', #14810, #30215, #3175, .T. ) ;
#19827=AXIS2_PLACEMENT_3D ( 'NONE', #2138, #7003, #16149 ) ;
#19857=EDGE_CURVE ( 'NONE', #5097, #16128, #14834, .T. ) ;
#19891=CARTESIAN_POINT ( 'NONE',  ( 0.8120000000000002771, 7.511012776518210972E-16, -5.000000000000000000 ) ) ;
#19902=ADVANCED_FACE ( 'NONE', ( #27099 ), #22660, .T. ) ;
#19994=LINE ( 'NONE', #1695, #14893 ) ;
#20010=CARTESIAN_POINT ( 'NONE',  ( 75.00000000000000000, 6.901118539064950623E-16, -4.188000000000025480 ) ) ;
#20035=FILL_AREA_STYLE_COLOUR ( '', #24332 ) ;
#20088=DIRECTION ( 'NONE',  ( 0.9773680663943725699, 5.871577894680254031E-18, -0.2115458881484706954 ) ) ;
#20190=ORIENTED_EDGE ( 'NONE', *, *, #11445, .F. ) ;
#20207=DIRECTION ( 'NONE',  ( -1.000000000000000000, 0.000000000000000000, 0.000000000000000000 ) ) ;
#20325=DIRECTION ( 'NONE',  ( 1.000000000000000000, 0.000000000000000000, 0.000000000000000000 ) ) ;
#20403=VERTEX_POINT ( 'NONE', #12229 ) ;
#20468=ORIENTED_EDGE ( 'NONE', *, *, #9795, .T. ) ;
#20485=UNCERTAINTY_MEASURE_WITH_UNIT (LENGTH_MEASURE( 1.000000000000000082E-05 ), #16538, 'distance_accuracy_value', 'NONE');
#20510=CARTESIAN_POINT ( 'NONE',  ( -1.310841663519413114, 7.511012776518212944E-16, -5.000000000000000888 ) ) ;
#20560=ORIENTED_EDGE ( 'NONE', *, *, #6232, .F. ) ;
#20640=CARTESIAN_POINT ( 'NONE',  ( 49.00000000000000000, 0.000000000000000000, 0.000000000000000000 ) ) ;
#20642=ORIENTED_EDGE ( 'NONE', *, *, #15294, .T. ) ;
#20671=DIRECTION ( 'NONE',  ( 1.000000000000000000, 0.000000000000000000, 0.000000000000000000 ) ) ;
#20753=CYLINDRICAL_SURFACE ( 'NONE', #27394, 5.000000000000000000 ) ;
#20814=ADVANCED_FACE ( 'NONE', ( #4436 ), #4158, .T. ) ;
#20865=ORIENTED_EDGE ( 'NONE', *, *, #19857, .T. ) ;
#20888=( NAMED_UNIT ( * ) SI_UNIT ( $, .STERADIAN. ) SOLID_ANGLE_UNIT ( ) );
#21007=ORIENTED_EDGE ( 'NONE', *, *, #11512, .T. ) ;
#21093=ADVANCED_FACE ( 'NONE', ( #22540 ), #283, .T. ) ;
#21175=FACE_OUTER_BOUND ( 'NONE', #1867, .T. ) ;
#21217=ORIENTED_EDGE ( 'NONE', *, *, #25073, .F. ) ;
#21250=DIRECTION ( 'NONE',  ( -1.000000000000000000, 0.000000000000000000, -0.000000000000000000 ) ) ;
#21266=ADVANCED_FACE ( 'NONE', ( #4961 ), #6614, .T. ) ;
#21278=ADVANCED_FACE ( 'NONE', ( #23582 ), #24664, .T. ) ;
#21327=ORIENTED_EDGE ( 'NONE', *, *, #2615, .T. ) ;
#21332=EDGE_LOOP ( 'NONE', ( #7650, #20468, #7792, #3636 ) ) ;
#21342=ADVANCED_FACE ( 'NONE', ( #21887 ), #17345, .T. ) ;
#21409=CARTESIAN_POINT ( 'NONE',  ( 15.00000000000000000, 0.000000000000000000, 0.000000000000000000 ) ) ;
#21414=EDGE_LOOP ( 'NONE', ( #21327, #19130 ) ) ;
#21682=AXIS2_PLACEMENT_3D ( 'NONE', #13020, #15605, #6311 ) ;
#21701=CARTESIAN_POINT ( 'NONE',  ( 74.18800000000001660, 0.000000000000000000, 0.000000000000000000 ) ) ;
#21765=EDGE_CURVE ( 'NONE', #12978, #25256, #19994, .T. ) ;
#21864=EDGE_CURVE ( 'NONE', #2741, #21885, #8686, .T. ) ;
#21885=VERTEX_POINT ( 'NONE', #27213 ) ;
#21887=FACE_OUTER_BOUND ( 'NONE', #17132, .T. ) ;
#21936=ADVANCED_FACE ( 'NONE', ( #26904 ), #3673, .T. ) ;
#22100=FACE_OUTER_BOUND ( 'NONE', #4073, .T. ) ;
#22137=EDGE_CURVE ( 'NONE', #9311, #25636, #6610, .T. ) ;
#22219=DIRECTION ( 'NONE',  ( -0.9773680663943724589, 3.177847737406115317E-17, -0.2115458881484709175 ) ) ;
#22234=AXIS2_PLACEMENT_3D ( 'NONE', #16714, #28812, #5418 ) ;
#22351=ORIENTED_EDGE ( 'NONE', *, *, #10348, .F. ) ;
#22494=DIRECTION ( 'NONE',  ( 0.000000000000000000, 2.775557561562890735E-17, -1.000000000000000000 ) ) ;
#22516=PLANE ( 'NONE',  #9117 ) ;
#22540=FACE_OUTER_BOUND ( 'NONE', #4111, .T. ) ;
#22549=EDGE_LOOP ( 'NONE', ( #17718, #9439, #4300, #5656 ) ) ;
#22561=CIRCLE ( 'NONE', #17184, 5.000000000000000888 ) ;
#22581=DIRECTION ( 'NONE',  ( 0.000000000000000000, -2.775557561562890735E-17, 1.000000000000000000 ) ) ;
#22660=CONICAL_SURFACE ( 'NONE', #7057, 5.000000000000000000, 0.2131563744996336218 ) ;
#22741=DIRECTION ( 'NONE',  ( -1.000000000000000000, 0.000000000000000000, -0.000000000000000000 ) ) ;
#22805=VERTEX_POINT ( 'NONE', #20010 ) ;
#22861=AXIS2_PLACEMENT_3D ( 'NONE', #1937, #15790, #18387 ) ;
#23011=EDGE_CURVE ( 'NONE', #705, #21885, #15929, .T. ) ;
#23064=VERTEX_POINT ( 'NONE', #29144 ) ;
#23095=DIRECTION ( 'NONE',  ( 0.9773680663943724589, 2.003532158470062816E-17, 0.2115458881484709175 ) ) ;
#23215=CIRCLE ( 'NONE', #10037, 5.000000000000000888 ) ;
#23218=EDGE_LOOP ( 'NONE', ( #25101, #21007, #586, #20190 ) ) ;
#23335=DIRECTION ( 'NONE',  ( -1.000000000000000000, 0.000000000000000000, -0.000000000000000000 ) ) ;
#23415=ORIENTED_EDGE ( 'NONE', *, *, #6232, .T. ) ;
#23439=ORIENTED_EDGE ( 'NONE', *, *, #3314, .F. ) ;
#23582=FACE_OUTER_BOUND ( 'NONE', #25151, .T. ) ;
#23622=DIRECTION ( 'NONE',  ( 0.000000000000000000, 2.775557561562890735E-17, -1.000000000000000000 ) ) ;
#23629=EDGE_CURVE ( 'NONE', #21885, #705, #30092, .T. ) ;
#23717=SHAPE_REPRESENTATION_RELATIONSHIP ( 'NONE' , 'NONE' ,  #29092, #21 ) ;
#23800=CYLINDRICAL_SURFACE ( 'NONE', #11323, 5.000000000000000888 ) ;
#23819=ORIENTED_EDGE ( 'NONE', *, *, #21864, .F. ) ;
#23833=ORIENTED_EDGE ( 'NONE', *, *, #28701, .F. ) ;
#23841=STYLED_ITEM ( 'NONE', ( #151 ), #979 ) ;
#23882=ORIENTED_EDGE ( 'NONE', *, *, #15060, .F. ) ;
#23928=CIRCLE ( 'NONE', #27851, 4.188000000000025480 ) ;
#24038=DIRECTION ( 'NONE',  ( 0.000000000000000000, 2.775557561562890735E-17, -1.000000000000000000 ) ) ;
#24110=ADVANCED_FACE ( 'NONE', ( #26002 ), #6186, .T. ) ;
#24180=EDGE_CURVE ( 'NONE', #25256, #20403, #23215, .T. ) ;
#24270=CARTESIAN_POINT ( 'NONE',  ( -1.310841663519413114, 7.511012776518211958E-16, -5.000000000000000000 ) ) ;
#24332=COLOUR_RGB ( '', 0.09019608, 0.27058824, 0.51372549) ;
#24515=DIRECTION ( 'NONE',  ( 0.000000000000000000, 2.775557561562890735E-17, -1.000000000000000000 ) ) ;
#24664=CONICAL_SURFACE ( 'NONE', #14872, 5.000000000000000888, 0.2131563744996338439 ) ;
#24766=ORIENTED_EDGE ( 'NONE', *, *, #21864, .T. ) ;
#24776=EDGE_CURVE ( 'NONE', #2878, #5097, #5800, .T. ) ;
#24790=CONICAL_SURFACE ( 'NONE', #7232, 4.513000000000000789, 0.2131563744996339549 ) ;
#24857=STYLED_ITEM ( 'NONE', ( #26166 ), #21 ) ;
#24927=( GEOMETRIC_REPRESENTATION_CONTEXT ( 3 ) GLOBAL_UNCERTAINTY_ASSIGNED_CONTEXT ( ( #20485 ) ) GLOBAL_UNIT_ASSIGNED_CONTEXT ( ( #16538, #72, #11491 ) ) REPRESENTATION_CONTEXT ( 'NONE', 'WORKASPACE' ) );
#25073=EDGE_CURVE ( 'NONE', #25256, #25636, #15700, .T. ) ;
#25080=LINE ( 'NONE', #8883, #5358 ) ;
#25101=ORIENTED_EDGE ( 'NONE', *, *, #29173, .F. ) ;
#25151=EDGE_LOOP ( 'NONE', ( #982, #8223, #8751, #25709 ) ) ;
#25212=ADVANCED_FACE ( 'NONE', ( #21175 ), #7149, .F. ) ;
#25253=CARTESIAN_POINT ( 'NONE',  ( 49.00000000000000000, -1.387778780781445676E-16, 5.000000000000000888 ) ) ;
#25256=VERTEX_POINT ( 'NONE', #16604 ) ;
#25273=DIRECTION ( 'NONE',  ( 0.000000000000000000, 2.775557561562890735E-17, -1.000000000000000000 ) ) ;
#25275=DIRECTION ( 'NONE',  ( 0.000000000000000000, -2.775557561562890735E-17, 1.000000000000000000 ) ) ;
#25304=ORIENTED_EDGE ( 'NONE', *, *, #9721, .T. ) ;
#25353=CARTESIAN_POINT ( 'NONE',  ( -1.310841663519413114, 0.000000000000000000, 0.000000000000000000 ) ) ;
#25374=CARTESIAN_POINT ( 'NONE',  ( 75.00000000000000000, 0.000000000000000000, 0.000000000000000000 ) ) ;
#25386=VECTOR ( 'NONE', #18019, 1000.000000000000000 ) ;
#25449=ADVANCED_FACE ( 'NONE', ( #12737 ), #22516, .F. ) ;
#25487=FACE_OUTER_BOUND ( 'NONE', #26782, .T. ) ;
#25546=ADVANCED_FACE ( 'NONE', ( #27573 ), #2342, .T. ) ;
#25628=AXIS2_PLACEMENT_3D ( 'NONE', #14251, #20671, #25273 ) ;
#25636=VERTEX_POINT ( 'NONE', #25253 ) ;
#25691=DIRECTION ( 'NONE',  ( 0.000000000000000000, 2.775557561562890735E-17, -1.000000000000000000 ) ) ;
#25705=FILL_AREA_STYLE_COLOUR ( '', #29861 ) ;
#25709=ORIENTED_EDGE ( 'NONE', *, *, #11445, .T. ) ;
#25743=VECTOR ( 'NONE', #19391, 1000.000000000000114 ) ;
#25786=( LENGTH_UNIT ( ) NAMED_UNIT ( * ) SI_UNIT ( .MILLI., .METRE. ) );
#25897=ORIENTED_EDGE ( 'NONE', *, *, #29447, .T. ) ;
#25899=AXIS2_PLACEMENT_3D ( 'NONE', #13665, #8631, #25275 ) ;
#25936=ORIENTED_EDGE ( 'NONE', *, *, #23629, .F. ) ;
#25983=DIRECTION ( 'NONE',  ( 0.000000000000000000, -2.775557561562890735E-17, 1.000000000000000000 ) ) ;
#26002=FACE_OUTER_BOUND ( 'NONE', #5248, .T. ) ;
#26012=DIRECTION ( 'NONE',  ( 0.000000000000000000, 2.775557561562890735E-17, -1.000000000000000000 ) ) ;
#26103=AXIS2_PLACEMENT_3D ( 'NONE', #6886, #13732, #18467 ) ;
#26145=AXIS2_PLACEMENT_3D ( 'NONE', #15012, #3438, #12731 ) ;
#26166=PRESENTATION_STYLE_ASSIGNMENT (( #28183 ) ) ;
#26209=CARTESIAN_POINT ( 'NONE',  ( 13.87499999999999822, 0.000000000000000000, 0.000000000000000000 ) ) ;
#26239=CARTESIAN_POINT ( 'NONE',  ( 15.00000000000000000, 4.735455214955320607E-16, 5.000000000000000000 ) ) ;
#26340=DIRECTION ( 'NONE',  ( 0.000000000000000000, -2.775557561562890735E-17, 1.000000000000000000 ) ) ;
#26482=AXIS2_PLACEMENT_3D ( 'NONE', #13086, #12784, #15528 ) ;
#26521=CONICAL_SURFACE ( 'NONE', #27051, 4.187999999999997947, 0.7853981633974482790 ) ;
#26548=LINE ( 'NONE', #17069, #18488 ) ;
#26586=LINE ( 'NONE', #11501, #25743 ) ;
#26615=AXIS2_PLACEMENT_3D ( 'NONE', #29765, #15795, #11072 ) ;
#26664=AXIS2_PLACEMENT_3D ( 'NONE', #11287, #3829, #6267 ) ;
#26738=VERTEX_POINT ( 'NONE', #3822 ) ;
#26756=EDGE_LOOP ( 'NONE', ( #5653, #18699, #12507, #2727 ) ) ;
#26782=EDGE_LOOP ( 'NONE', ( #23819, #18399, #17421, #25936 ) ) ;
#26786=ADVANCED_FACE ( 'NONE', ( #27050 ), #24790, .T. ) ;
#26789=EDGE_CURVE ( 'NONE', #23064, #2741, #15516, .T. ) ;
#26904=FACE_OUTER_BOUND ( 'NONE', #6968, .T. ) ;
#26920=CYLINDRICAL_SURFACE ( 'NONE', #1838, 5.000000000000000888 ) ;
#27050=FACE_OUTER_BOUND ( 'NONE', #21332, .T. ) ;
#27051=AXIS2_PLACEMENT_3D ( 'NONE', #1736, #20325, #29714 ) ;
#27099=FACE_OUTER_BOUND ( 'NONE', #10179, .T. ) ;
#27121=CARTESIAN_POINT ( 'NONE',  ( 47.87499999999999289, 0.000000000000000000, 0.000000000000000000 ) ) ;
#27196=CIRCLE ( 'NONE', #16906, 5.000000000000000888 ) ;
#27197=CYLINDRICAL_SURFACE ( 'NONE', #11214, 5.000000000000000888 ) ;
#27213=CARTESIAN_POINT ( 'NONE',  ( 0.8120000000000002771, -1.387778780781445429E-16, 5.000000000000000000 ) ) ;
#27394=AXIS2_PLACEMENT_3D ( 'NONE', #25353, #4446, #11442 ) ;
#27447=CARTESIAN_POINT ( 'NONE',  ( 12.74999999999999822, 0.000000000000000000, 0.000000000000000000 ) ) ;
#27491=DIRECTION ( 'NONE',  ( 0.9773680663943724589, 5.871577894680259423E-18, -0.2115458881484709175 ) ) ;
#27573=FACE_OUTER_BOUND ( 'NONE', #29056, .T. ) ;
#27590=EDGE_CURVE ( 'NONE', #23064, #705, #7546, .T. ) ;
#27596=CARTESIAN_POINT ( 'NONE',  ( 15.00000000000000000, 1.387778780781445429E-16, -5.000000000000000000 ) ) ;
#27599=CARTESIAN_POINT ( 'NONE',  ( 15.00000000000000000, -1.252609127533332839E-16, 4.513000000000000789 ) ) ;
#27713=DIRECTION ( 'NONE',  ( 0.000000000000000000, -2.775557561562890735E-17, 1.000000000000000000 ) ) ;
#27806=VECTOR ( 'NONE', #14171, 1000.000000000000114 ) ;
#27851=AXIS2_PLACEMENT_3D ( 'NONE', #4869, #14166, #2601 ) ;
#27898=DIRECTION ( 'NONE',  ( 0.000000000000000000, 2.775557561562890735E-17, -1.000000000000000000 ) ) ;
#28031=EDGE_LOOP ( 'NONE', ( #13587, #3169, #6772, #20560 ) ) ;
#28183=SURFACE_STYLE_USAGE ( .BOTH. , #12105 ) ;
#28192=AXIS2_PLACEMENT_3D ( 'NONE', #25374, #4760, #13758 ) ;
#28195=CARTESIAN_POINT ( 'NONE',  ( 0.000000000000000000, 1.162403506782538081E-16, -4.187999999999997947 ) ) ;
#28205=LINE ( 'NONE', #11666, #2045 ) ;
#28279=EDGE_LOOP ( 'NONE', ( #18571, #11237, #10496, #1834 ) ) ;
#28436=ORIENTED_EDGE ( 'NONE', *, *, #9795, .F. ) ;
#28701=EDGE_CURVE ( 'NONE', #9311, #10747, #311, .T. ) ;
#28812=DIRECTION ( 'NONE',  ( -1.000000000000000000, 0.000000000000000000, -0.000000000000000000 ) ) ;
#28914=CARTESIAN_POINT ( 'NONE',  ( 75.00000000000000000, -1.162403506782545970E-16, 4.188000000000025480 ) ) ;
#29022=ORIENTED_EDGE ( 'NONE', *, *, #23011, .F. ) ;
#29056=EDGE_LOOP ( 'NONE', ( #16642, #24766, #29022, #17417 ) ) ;
#29092=SHAPE_REPRESENTATION ( 'double end studs bm=1.5d_am_AM A M10X60-N', ( #13190 ), #8326 ) ;
#29143=CARTESIAN_POINT ( 'NONE',  ( 49.00000000000000000, 0.000000000000000000, 0.000000000000000000 ) ) ;
#29144=CARTESIAN_POINT ( 'NONE',  ( 0.000000000000000000, 1.162403506782538081E-16, -4.187999999999997947 ) ) ;
#29173=EDGE_CURVE ( 'NONE', #20403, #26738, #16892, .T. ) ;
#29297=AXIS2_PLACEMENT_3D ( 'NONE', #29143, #10014, #12762 ) ;
#29401=EDGE_CURVE ( 'NONE', #25636, #26738, #10233, .T. ) ;
#29447=EDGE_CURVE ( 'NONE', #30215, #14937, #17198, .T. ) ;
#29460=CARTESIAN_POINT ( 'NONE',  ( 47.87499999999999289, 7.328119615409992624E-16, -4.756499999999998174 ) ) ;
#29606=CARTESIAN_POINT ( 'NONE',  ( 74.18800000000001660, 0.000000000000000000, 0.000000000000000000 ) ) ;
#29628=DIRECTION ( 'NONE',  ( -1.000000000000000000, 0.000000000000000000, -0.000000000000000000 ) ) ;
#29714=DIRECTION ( 'NONE',  ( 0.000000000000000000, 2.775557561562890735E-17, -1.000000000000000000 ) ) ;
#29765=CARTESIAN_POINT ( 'NONE',  ( 15.00000000000000000, 0.000000000000000000, 0.000000000000000000 ) ) ;
#29861=COLOUR_RGB ( '', 0.09019608, 0.27058824, 0.51372549) ;
#29961=EDGE_CURVE ( 'NONE', #22805, #12978, #23928, .T. ) ;
#29962=CARTESIAN_POINT ( 'NONE',  ( -1.310841663519413114, -1.387778780781445676E-16, 5.000000000000000888 ) ) ;
#29968=DIRECTION ( 'NONE',  ( -1.000000000000000000, -0.000000000000000000, -0.000000000000000000 ) ) ;
#30023=DIRECTION ( 'NONE',  ( -1.000000000000000000, 0.000000000000000000, -0.000000000000000000 ) ) ;
#30072=ORIENTED_EDGE ( 'NONE', *, *, #14851, .T. ) ;
#30092=CIRCLE ( 'NONE', #26145, 5.000000000000000888 ) ;
#30189=DIRECTION ( 'NONE',  ( -1.000000000000000000, 0.000000000000000000, -0.000000000000000000 ) ) ;
#30215=VERTEX_POINT ( 'NONE', #4096 ) ;
#30246=DIRECTION ( 'NONE',  ( -1.000000000000000000, 0.000000000000000000, -0.000000000000000000 ) ) ;
#30262=( NAMED_UNIT ( * ) PLANE_ANGLE_UNIT ( ) SI_UNIT ( $, .RADIAN. ) );
ENDSEC;
END-ISO-10303-21;
